ISO-10303-21;
HEADER;
/* Generated by software containing ST-Developer
 * from STEP Tools, Inc. (www.steptools.com) 
 */
/* OPTION: using custom renumber hook */

FILE_DESCRIPTION(
/* description */ ('STEP AP242 Edition 2', 'CAx-IF Rec.Pracs.---Representation and Presentation of Product Manufa
cturing Information (PMI)---4.0---2014-10-13', 'CAx-IF Rec.Pracs.---3D Tessellated Geometry---0.4---2014-09-14', '2;1', 'CAx-IF Rec.Pracs.---User Defined Attributes---1.5---2016-08-15'),
/* implementation_level */ '2;1');

FILE_NAME(
/* name */ 'Part 3.step',
/* time_stamp */ '2026-10-09T13:59:33Z',
/* author */ (''),
/* organization */ (''),
/* preprocessor_version */ 'ST-DEVELOPER v20',
/* originating_system */ 'ONSHAPE BY PTC INC, 1.221',
/* authorisation */ '  ');

FILE_SCHEMA (('AP242_MANAGED_MODEL_BASED_3D_ENGINEERING_MIM_LF { 1 0 10303 442 3 1 4 }'));
ENDSEC;

DATA;
#164=LINE('',#9106,#448);
#165=LINE('',#9110,#449);
#166=LINE('',#9117,#450);
#167=LINE('',#9121,#451);
#168=LINE('',#9125,#452);
#169=LINE('',#9126,#453);
#170=LINE('',#9128,#454);
#171=LINE('',#9130,#455);
#448=VECTOR('',#7242,1.);
#449=VECTOR('',#7245,1.);
#450=VECTOR('',#7252,1.);
#451=VECTOR('',#7255,1.);
#452=VECTOR('',#7260,1.);
#453=VECTOR('',#7261,1.);
#454=VECTOR('',#7264,1.);
#455=VECTOR('',#7267,1.);
#675=SHAPE_REPRESENTATION_RELATIONSHIP('','',#5693,#689);
#689=ADVANCED_BREP_SHAPE_REPRESENTATION('',(#5662),#10147);
#741=PLANE('',#6004);
#742=PLANE('',#6010);
#743=PLANE('',#6015);
#744=PLANE('',#6017);
#745=PLANE('',#6019);
#746=PLANE('',#6025);
#747=PLANE('',#6026);
#748=PLANE('',#6032);
#1432=ORIENTED_EDGE('',*,*,#2653,.F.);
#1433=ORIENTED_EDGE('',*,*,#2654,.F.);
#1434=ORIENTED_EDGE('',*,*,#2655,.T.);
#1435=ORIENTED_EDGE('',*,*,#2656,.T.);
#1436=ORIENTED_EDGE('',*,*,#2657,.T.);
#1437=ORIENTED_EDGE('',*,*,#2658,.T.);
#1438=ORIENTED_EDGE('',*,*,#2659,.F.);
#1439=ORIENTED_EDGE('',*,*,#2660,.F.);
#1440=ORIENTED_EDGE('',*,*,#2661,.F.);
#1441=ORIENTED_EDGE('',*,*,#2662,.F.);
#1442=ORIENTED_EDGE('',*,*,#2663,.F.);
#1443=ORIENTED_EDGE('',*,*,#2664,.T.);
#1444=ORIENTED_EDGE('',*,*,#2660,.T.);
#1445=ORIENTED_EDGE('',*,*,#2665,.F.);
#1446=ORIENTED_EDGE('',*,*,#2655,.F.);
#1447=ORIENTED_EDGE('',*,*,#2666,.T.);
#1448=ORIENTED_EDGE('',*,*,#2663,.T.);
#1449=ORIENTED_EDGE('',*,*,#2667,.F.);
#1450=ORIENTED_EDGE('',*,*,#2656,.F.);
#1451=ORIENTED_EDGE('',*,*,#2665,.T.);
#1452=ORIENTED_EDGE('',*,*,#2662,.T.);
#1453=ORIENTED_EDGE('',*,*,#2668,.F.);
#1454=ORIENTED_EDGE('',*,*,#2657,.F.);
#1455=ORIENTED_EDGE('',*,*,#2667,.T.);
#1456=ORIENTED_EDGE('',*,*,#2661,.T.);
#1457=ORIENTED_EDGE('',*,*,#2666,.F.);
#1458=ORIENTED_EDGE('',*,*,#2658,.F.);
#1459=ORIENTED_EDGE('',*,*,#2668,.T.);
#1460=ORIENTED_EDGE('',*,*,#2659,.T.);
#1461=ORIENTED_EDGE('',*,*,#2664,.F.);
#1462=ORIENTED_EDGE('',*,*,#2669,.T.);
#1463=ORIENTED_EDGE('',*,*,#2670,.F.);
#1464=ORIENTED_EDGE('',*,*,#2669,.F.);
#1465=ORIENTED_EDGE('',*,*,#2654,.T.);
#1466=ORIENTED_EDGE('',*,*,#2670,.T.);
#1467=ORIENTED_EDGE('',*,*,#2671,.T.);
#1468=ORIENTED_EDGE('',*,*,#2671,.F.);
#1469=ORIENTED_EDGE('',*,*,#2672,.T.);
#1470=ORIENTED_EDGE('',*,*,#2673,.F.);
#1471=ORIENTED_EDGE('',*,*,#2672,.F.);
#1472=ORIENTED_EDGE('',*,*,#2653,.T.);
#1473=ORIENTED_EDGE('',*,*,#2673,.T.);
#1474=ORIENTED_EDGE('',*,*,#2674,.T.);
#1475=ORIENTED_EDGE('',*,*,#2674,.F.);
#2653=EDGE_CURVE('',#3323,#3323,#3818,.T.);
#2654=EDGE_CURVE('',#3324,#3324,#3819,.T.);
#2655=EDGE_CURVE('',#3325,#3326,#3820,.T.);
#2656=EDGE_CURVE('',#3326,#3327,#164,.T.);
#2657=EDGE_CURVE('',#3327,#3328,#3821,.T.);
#2658=EDGE_CURVE('',#3328,#3325,#165,.T.);
#2659=EDGE_CURVE('',#3329,#3329,#3822,.T.);
#2660=EDGE_CURVE('',#3330,#3331,#3823,.T.);
#2661=EDGE_CURVE('',#3332,#3330,#166,.T.);
#2662=EDGE_CURVE('',#3333,#3332,#3824,.T.);
#2663=EDGE_CURVE('',#3331,#3333,#167,.T.);
#2664=EDGE_CURVE('',#3334,#3334,#3825,.T.);
#2665=EDGE_CURVE('',#3326,#3331,#168,.T.);
#2666=EDGE_CURVE('',#3325,#3330,#169,.T.);
#2667=EDGE_CURVE('',#3327,#3333,#170,.T.);
#2668=EDGE_CURVE('',#3328,#3332,#171,.T.);
#2669=EDGE_CURVE('',#3335,#3335,#3826,.T.);
#2670=EDGE_CURVE('',#3336,#3336,#3827,.T.);
#2671=EDGE_CURVE('',#3337,#3337,#3828,.F.);
#2672=EDGE_CURVE('',#3338,#3338,#3829,.T.);
#2673=EDGE_CURVE('',#3339,#3339,#3830,.T.);
#2674=EDGE_CURVE('',#3340,#3340,#3831,.F.);
#3323=VERTEX_POINT('',#9100);
#3324=VERTEX_POINT('',#9102);
#3325=VERTEX_POINT('',#9104);
#3326=VERTEX_POINT('',#9105);
#3327=VERTEX_POINT('',#9107);
#3328=VERTEX_POINT('',#9109);
#3329=VERTEX_POINT('',#9112);
#3330=VERTEX_POINT('',#9115);
#3331=VERTEX_POINT('',#9116);
#3332=VERTEX_POINT('',#9118);
#3333=VERTEX_POINT('',#9120);
#3334=VERTEX_POINT('',#9123);
#3335=VERTEX_POINT('',#9135);
#3336=VERTEX_POINT('',#9137);
#3337=VERTEX_POINT('',#9141);
#3338=VERTEX_POINT('',#9145);
#3339=VERTEX_POINT('',#9147);
#3340=VERTEX_POINT('',#9151);
#3818=CIRCLE('',#6005,0.002);
#3819=CIRCLE('',#6006,0.002);
#3820=CIRCLE('',#6007,0.003);
#3821=CIRCLE('',#6008,0.003);
#3822=CIRCLE('',#6009,0.0025);
#3823=CIRCLE('',#6011,0.003);
#3824=CIRCLE('',#6012,0.003);
#3825=CIRCLE('',#6013,0.0025);
#3826=CIRCLE('',#6020,0.002);
#3827=CIRCLE('',#6021,0.0015);
#3828=CIRCLE('',#6024,0.0015);
#3829=CIRCLE('',#6027,0.002);
#3830=CIRCLE('',#6028,0.0015);
#3831=CIRCLE('',#6031,0.0015);
#4270=EDGE_LOOP('',(#1432));
#4271=EDGE_LOOP('',(#1433));
#4272=EDGE_LOOP('',(#1434,#1435,#1436,#1437));
#4273=EDGE_LOOP('',(#1438));
#4274=EDGE_LOOP('',(#1439,#1440,#1441,#1442));
#4275=EDGE_LOOP('',(#1443));
#4276=EDGE_LOOP('',(#1444,#1445,#1446,#1447));
#4277=EDGE_LOOP('',(#1448,#1449,#1450,#1451));
#4278=EDGE_LOOP('',(#1452,#1453,#1454,#1455));
#4279=EDGE_LOOP('',(#1456,#1457,#1458,#1459));
#4280=EDGE_LOOP('',(#1460));
#4281=EDGE_LOOP('',(#1461));
#4282=EDGE_LOOP('',(#1462));
#4283=EDGE_LOOP('',(#1463));
#4284=EDGE_LOOP('',(#1464));
#4285=EDGE_LOOP('',(#1465));
#4286=EDGE_LOOP('',(#1466));
#4287=EDGE_LOOP('',(#1467));
#4288=EDGE_LOOP('',(#1468));
#4289=EDGE_LOOP('',(#1469));
#4290=EDGE_LOOP('',(#1470));
#4291=EDGE_LOOP('',(#1471));
#4292=EDGE_LOOP('',(#1472));
#4293=EDGE_LOOP('',(#1473));
#4294=EDGE_LOOP('',(#1474));
#4295=EDGE_LOOP('',(#1475));
#4718=FACE_BOUND('',#4270,.T.);
#4719=FACE_BOUND('',#4271,.T.);
#4720=FACE_BOUND('',#4272,.T.);
#4721=FACE_BOUND('',#4273,.T.);
#4722=FACE_BOUND('',#4274,.T.);
#4723=FACE_BOUND('',#4275,.T.);
#4724=FACE_BOUND('',#4276,.T.);
#4725=FACE_BOUND('',#4277,.T.);
#4726=FACE_BOUND('',#4278,.T.);
#4727=FACE_BOUND('',#4279,.T.);
#4728=FACE_BOUND('',#4280,.T.);
#4729=FACE_BOUND('',#4281,.T.);
#4730=FACE_BOUND('',#4282,.T.);
#4731=FACE_BOUND('',#4283,.T.);
#4732=FACE_BOUND('',#4284,.T.);
#4733=FACE_BOUND('',#4285,.T.);
#4734=FACE_BOUND('',#4286,.T.);
#4735=FACE_BOUND('',#4287,.T.);
#4736=FACE_BOUND('',#4288,.T.);
#4737=FACE_BOUND('',#4289,.T.);
#4738=FACE_BOUND('',#4290,.T.);
#4739=FACE_BOUND('',#4291,.T.);
#4740=FACE_BOUND('',#4292,.T.);
#4741=FACE_BOUND('',#4293,.T.);
#4742=FACE_BOUND('',#4294,.T.);
#4743=FACE_BOUND('',#4295,.T.);
#5079=CYLINDRICAL_SURFACE('',#6014,0.003);
#5080=CYLINDRICAL_SURFACE('',#6016,0.003);
#5081=CYLINDRICAL_SURFACE('',#6018,0.0025);
#5082=CYLINDRICAL_SURFACE('',#6022,0.002);
#5083=CYLINDRICAL_SURFACE('',#6023,0.0015);
#5084=CYLINDRICAL_SURFACE('',#6029,0.002);
#5085=CYLINDRICAL_SURFACE('',#6030,0.0015);
#5338=ADVANCED_FACE('',(#4718,#4719,#4720,#4721),#741,.T.);
#5339=ADVANCED_FACE('',(#4722,#4723),#742,.F.);
#5340=ADVANCED_FACE('',(#4724),#5079,.T.);
#5341=ADVANCED_FACE('',(#4725),#743,.F.);
#5342=ADVANCED_FACE('',(#4726),#5080,.T.);
#5343=ADVANCED_FACE('',(#4727),#744,.F.);
#5344=ADVANCED_FACE('',(#4728,#4729),#5081,.F.);
#5345=ADVANCED_FACE('',(#4730,#4731),#745,.T.);
#5346=ADVANCED_FACE('',(#4732,#4733),#5082,.T.);
#5347=ADVANCED_FACE('',(#4734,#4735),#5083,.F.);
#5348=ADVANCED_FACE('',(#4736),#746,.T.);
#5349=ADVANCED_FACE('',(#4737,#4738),#747,.T.);
#5350=ADVANCED_FACE('',(#4739,#4740),#5084,.T.);
#5351=ADVANCED_FACE('',(#4741,#4742),#5085,.F.);
#5352=ADVANCED_FACE('',(#4743),#748,.T.);
#5543=CLOSED_SHELL('',(#5338,#5339,#5340,#5341,#5342,#5343,#5344,#5345,
#5346,#5347,#5348,#5349,#5350,#5351,#5352));
#5557=STYLED_ITEM('',(#5571),#5662);
#5571=PRESENTATION_STYLE_ASSIGNMENT((#5585));
#5585=SURFACE_STYLE_USAGE(.BOTH.,#5599);
#5599=SURFACE_SIDE_STYLE('',(#5613));
#5613=SURFACE_STYLE_FILL_AREA(#5627);
#5627=FILL_AREA_STYLE('',(#5641));
#5641=FILL_AREA_STYLE_COLOUR('',#5653);
#5653=COLOUR_RGB('', 0.40784314, 0.44705882, 0.49803922);
#5662=MANIFOLD_SOLID_BREP('Part 3',#5543);
#5677=SHAPE_DEFINITION_REPRESENTATION(#10188,#5693);
#5693=SHAPE_REPRESENTATION('Part 3',(#5704),#10147);
#5704=AXIS2_PLACEMENT_3D('',#8391,#6505,#6506);
#6004=AXIS2_PLACEMENT_3D('',#9098,#7234,#7235);
#6005=AXIS2_PLACEMENT_3D('',#9099,#7236,#7237);
#6006=AXIS2_PLACEMENT_3D('',#9101,#7238,#7239);
#6007=AXIS2_PLACEMENT_3D('',#9103,#7240,#7241);
#6008=AXIS2_PLACEMENT_3D('',#9108,#7243,#7244);
#6009=AXIS2_PLACEMENT_3D('',#9111,#7246,#7247);
#6010=AXIS2_PLACEMENT_3D('',#9113,#7248,#7249);
#6011=AXIS2_PLACEMENT_3D('',#9114,#7250,#7251);
#6012=AXIS2_PLACEMENT_3D('',#9119,#7253,#7254);
#6013=AXIS2_PLACEMENT_3D('',#9122,#7256,#7257);
#6014=AXIS2_PLACEMENT_3D('',#9124,#7258,#7259);
#6015=AXIS2_PLACEMENT_3D('',#9127,#7262,#7263);
#6016=AXIS2_PLACEMENT_3D('',#9129,#7265,#7266);
#6017=AXIS2_PLACEMENT_3D('',#9131,#7268,#7269);
#6018=AXIS2_PLACEMENT_3D('',#9132,#7270,#7271);
#6019=AXIS2_PLACEMENT_3D('',#9133,#7272,#7273);
#6020=AXIS2_PLACEMENT_3D('',#9134,#7274,#7275);
#6021=AXIS2_PLACEMENT_3D('',#9136,#7276,#7277);
#6022=AXIS2_PLACEMENT_3D('',#9138,#7278,#7279);
#6023=AXIS2_PLACEMENT_3D('',#9139,#7280,#7281);
#6024=AXIS2_PLACEMENT_3D('',#9140,#7282,#7283);
#6025=AXIS2_PLACEMENT_3D('',#9142,#7284,#7285);
#6026=AXIS2_PLACEMENT_3D('',#9143,#7286,#7287);
#6027=AXIS2_PLACEMENT_3D('',#9144,#7288,#7289);
#6028=AXIS2_PLACEMENT_3D('',#9146,#7290,#7291);
#6029=AXIS2_PLACEMENT_3D('',#9148,#7292,#7293);
#6030=AXIS2_PLACEMENT_3D('',#9149,#7294,#7295);
#6031=AXIS2_PLACEMENT_3D('',#9150,#7296,#7297);
#6032=AXIS2_PLACEMENT_3D('',#9152,#7298,#7299);
#6505=DIRECTION('',(0.,0.,1.));
#6506=DIRECTION('',(1.,0.,0.));
#7234=DIRECTION('',(0.,1.,0.));
#7235=DIRECTION('',(0.,0.,1.));
#7236=DIRECTION('',(0.,1.,0.));
#7237=DIRECTION('',(1.,0.,0.));
#7238=DIRECTION('',(0.,1.,0.));
#7239=DIRECTION('',(1.,0.,0.));
#7240=DIRECTION('',(0.,1.,0.));
#7241=DIRECTION('',(0.,0.,1.));
#7242=DIRECTION('',(0.866025403784438,0.,0.5));
#7243=DIRECTION('',(0.,1.,0.));
#7244=DIRECTION('',(0.,0.,1.));
#7245=DIRECTION('',(-0.866025403784438,0.,-0.5));
#7246=DIRECTION('',(0.,1.,0.));
#7247=DIRECTION('',(0.,0.,1.));
#7248=DIRECTION('',(0.,1.,0.));
#7249=DIRECTION('',(0.,0.,1.));
#7250=DIRECTION('',(0.,1.,0.));
#7251=DIRECTION('',(0.,0.,1.));
#7252=DIRECTION('',(-0.866025403784438,0.,-0.5));
#7253=DIRECTION('',(0.,1.,0.));
#7254=DIRECTION('',(0.,0.,1.));
#7255=DIRECTION('',(0.866025403784438,0.,0.5));
#7256=DIRECTION('',(0.,1.,0.));
#7257=DIRECTION('',(0.,0.,1.));
#7258=DIRECTION('',(0.,-1.,0.));
#7259=DIRECTION('',(0.,0.,-1.));
#7260=DIRECTION('',(0.,-1.,0.));
#7261=DIRECTION('',(0.,-1.,0.));
#7262=DIRECTION('',(0.5,0.,-0.866025403784438));
#7263=DIRECTION('',(-0.866025403784438,0.,-0.5));
#7264=DIRECTION('',(0.,-1.,0.));
#7265=DIRECTION('',(0.,-1.,0.));
#7266=DIRECTION('',(0.,0.,-1.));
#7267=DIRECTION('',(0.,-1.,0.));
#7268=DIRECTION('',(-0.5,0.,0.866025403784438));
#7269=DIRECTION('',(0.866025403784438,0.,0.5));
#7270=DIRECTION('',(0.,-1.,0.));
#7271=DIRECTION('',(0.,0.,-1.));
#7272=DIRECTION('',(0.,1.,0.));
#7273=DIRECTION('',(0.,0.,1.));
#7274=DIRECTION('',(0.,1.,0.));
#7275=DIRECTION('',(1.,0.,0.));
#7276=DIRECTION('',(0.,1.,0.));
#7277=DIRECTION('',(0.,0.,1.));
#7278=DIRECTION('',(0.,-1.,0.));
#7279=DIRECTION('',(0.,0.,-1.));
#7280=DIRECTION('',(0.,-1.,0.));
#7281=DIRECTION('',(0.,0.,-1.));
#7282=DIRECTION('',(0.,1.,0.));
#7283=DIRECTION('',(0.,0.,1.));
#7284=DIRECTION('',(0.,1.,0.));
#7285=DIRECTION('',(0.,0.,1.));
#7286=DIRECTION('',(0.,1.,0.));
#7287=DIRECTION('',(0.,0.,1.));
#7288=DIRECTION('',(0.,1.,0.));
#7289=DIRECTION('',(1.,0.,0.));
#7290=DIRECTION('',(0.,1.,0.));
#7291=DIRECTION('',(0.,0.,1.));
#7292=DIRECTION('',(0.,-1.,0.));
#7293=DIRECTION('',(0.,0.,-1.));
#7294=DIRECTION('',(0.,-1.,0.));
#7295=DIRECTION('',(0.,0.,-1.));
#7296=DIRECTION('',(0.,1.,0.));
#7297=DIRECTION('',(0.,0.,1.));
#7298=DIRECTION('',(0.,1.,0.));
#7299=DIRECTION('',(0.,0.,1.));
#8391=CARTESIAN_POINT('',(0.,0.,0.));
#9098=CARTESIAN_POINT('',(0.,0.0075,0.));
#9099=CARTESIAN_POINT('',(0.00733163402696092,0.0075,0.00423292087906571));
#9100=CARTESIAN_POINT('',(0.00933163402696092,0.0075,0.00423292087906571));
#9101=CARTESIAN_POINT('',(0.0151423348616945,0.0075,0.00874243110855875));
#9102=CARTESIAN_POINT('',(0.0171423348616945,0.0075,0.00874243110855875));
#9103=CARTESIAN_POINT('',(0.,0.0075,0.));
#9104=CARTESIAN_POINT('',(0.0015,0.0075,-0.00259807621135332));
#9105=CARTESIAN_POINT('',(-0.0015,0.0075,0.00259807621135332));
#9106=CARTESIAN_POINT('',(-0.0015,0.0075,0.00259807621135332));
#9107=CARTESIAN_POINT('',(0.0136554445662277,0.0075,0.0113480762113533));
#9108=CARTESIAN_POINT('',(0.0151554445662277,0.0075,0.00875));
#9109=CARTESIAN_POINT('',(0.0166554445662276,0.0075,0.0061519237886467));
#9110=CARTESIAN_POINT('',(0.0015,0.0075,-0.00259807621135332));
#9111=CARTESIAN_POINT('',(0.,0.0075,0.));
#9112=CARTESIAN_POINT('',(0.,0.0075,0.0025));
#9113=CARTESIAN_POINT('',(0.,0.0065,0.));
#9114=CARTESIAN_POINT('',(0.,0.0065,0.));
#9115=CARTESIAN_POINT('',(0.0015,0.0065,-0.00259807621135332));
#9116=CARTESIAN_POINT('',(-0.0015,0.0065,0.00259807621135332));
#9117=CARTESIAN_POINT('',(0.0015,0.0065,-0.00259807621135332));
#9118=CARTESIAN_POINT('',(0.0166554445662276,0.0065,0.0061519237886467));
#9119=CARTESIAN_POINT('',(0.0151554445662277,0.0065,0.00875));
#9120=CARTESIAN_POINT('',(0.0136554445662277,0.0065,0.0113480762113533));
#9121=CARTESIAN_POINT('',(-0.0015,0.0065,0.00259807621135332));
#9122=CARTESIAN_POINT('',(0.,0.0065,0.));
#9123=CARTESIAN_POINT('',(0.,0.0065,0.0025));
#9124=CARTESIAN_POINT('',(0.,0.0075,0.));
#9125=CARTESIAN_POINT('',(-0.0015,0.0075,0.00259807621135332));
#9126=CARTESIAN_POINT('',(0.0015,0.0075,-0.00259807621135332));
#9127=CARTESIAN_POINT('',(-0.0015,0.0075,0.00259807621135332));
#9128=CARTESIAN_POINT('',(0.0136554445662277,0.0075,0.0113480762113533));
#9129=CARTESIAN_POINT('',(0.0151554445662277,0.0075,0.00875));
#9130=CARTESIAN_POINT('',(0.0166554445662276,0.0075,0.0061519237886467));
#9131=CARTESIAN_POINT('',(0.0015,0.0075,-0.00259807621135332));
#9132=CARTESIAN_POINT('',(0.,0.0075,0.));
#9133=CARTESIAN_POINT('',(0.0151423348616945,0.012,0.00874243110855875));
#9134=CARTESIAN_POINT('',(0.0151423348616945,0.012,0.00874243110855875));
#9135=CARTESIAN_POINT('',(0.0171423348616945,0.012,0.00874243110855875));
#9136=CARTESIAN_POINT('',(0.0151423348616945,0.012,0.00874243110855875));
#9137=CARTESIAN_POINT('',(0.0151423348616945,0.012,0.0102424311085587));
#9138=CARTESIAN_POINT('',(0.0151423348616945,0.012,0.00874243110855875));
#9139=CARTESIAN_POINT('',(0.0151423348616945,0.012,0.00874243110855875));
#9140=CARTESIAN_POINT('',(0.0151423348616945,0.0075,0.00874243110855875));
#9141=CARTESIAN_POINT('',(0.0151423348616945,0.0075,0.0102424311085587));
#9142=CARTESIAN_POINT('',(0.,0.0075,0.));
#9143=CARTESIAN_POINT('',(0.00733163402696092,0.012,0.00423292087906571));
#9144=CARTESIAN_POINT('',(0.00733163402696092,0.012,0.00423292087906571));
#9145=CARTESIAN_POINT('',(0.00933163402696092,0.012,0.00423292087906571));
#9146=CARTESIAN_POINT('',(0.00733163402696092,0.012,0.00423292087906571));
#9147=CARTESIAN_POINT('',(0.00733163402696092,0.012,0.0057329208790657));
#9148=CARTESIAN_POINT('',(0.00733163402696092,0.012,0.00423292087906571));
#9149=CARTESIAN_POINT('',(0.00733163402696092,0.012,0.00423292087906571));
#9150=CARTESIAN_POINT('',(0.00733163402696092,0.0075,0.00423292087906571));
#9151=CARTESIAN_POINT('',(0.00733163402696092,0.0075,0.0057329208790657));
#9152=CARTESIAN_POINT('',(0.,0.0075,0.));
#10141=MECHANICAL_DESIGN_GEOMETRIC_PRESENTATION_REPRESENTATION('',(#5557),#10142);
#10142=(
GEOMETRIC_REPRESENTATION_CONTEXT(3)
GLOBAL_UNCERTAINTY_ASSIGNED_CONTEXT((#10158))
GLOBAL_UNIT_ASSIGNED_CONTEXT((#10176,#10175,#10174))
REPRESENTATION_CONTEXT('MAS-674','TOP_LEVEL_ASSEMBLY_PART')
);
#10147=(
GEOMETRIC_REPRESENTATION_CONTEXT(3)
GLOBAL_UNCERTAINTY_ASSIGNED_CONTEXT((#10163))
GLOBAL_UNIT_ASSIGNED_CONTEXT((#10176,#10175,#10174))
REPRESENTATION_CONTEXT('Part 3','COMPONENT_PART')
);
#10158=UNCERTAINTY_MEASURE_WITH_UNIT(LENGTH_MEASURE(1.E-8),#10176,
'DISTANCE_ACCURACY_VALUE','Maximum Tolerance applied to model');
#10163=UNCERTAINTY_MEASURE_WITH_UNIT(LENGTH_MEASURE(1.E-8),#10176,
'DISTANCE_ACCURACY_VALUE','Maximum Tolerance applied to model');
#10174=(
NAMED_UNIT(*)
SI_UNIT($,.STERADIAN.)
SOLID_ANGLE_UNIT()
);
#10175=(
NAMED_UNIT(*)
PLANE_ANGLE_UNIT()
SI_UNIT($,.RADIAN.)
);
#10176=(
LENGTH_UNIT()
NAMED_UNIT(*)
SI_UNIT($,.METRE.)
);
#10188=PRODUCT_DEFINITION_SHAPE('','',#10215);
#10215=PRODUCT_DEFINITION('','',#10247,#10231);
#10231=PRODUCT_DEFINITION_CONTEXT('',#10323,'design');
#10247=PRODUCT_DEFINITION_FORMATION_WITH_SPECIFIED_SOURCE('','',#10279,
 .NOT_KNOWN.);
#10279=PRODUCT('Part 3','Part 3','Part 3',(#10311));
#10311=PRODUCT_CONTEXT('',#10323,'mechanical');
#10323=APPLICATION_CONTEXT('managed model based 3d engineering');
ENDSEC;
END-ISO-10303-21;
